ISO-10303-21;
HEADER;
/* Generated by software containing ST-Developer
 * from STEP Tools, Inc. (www.steptools.com) 
 */

FILE_DESCRIPTION(
/* description */ ('Ball-type isolation valve (generic)'),
/* implementation_level */ '2;1');

FILE_NAME(
/* name */ 'Flat Washer - M5.step',
/* time_stamp */ '2026-10-27T10:53:05-07:00',
/* author */ (''),
/* organization */ (''),
/* preprocessor_version */ 'ST-DEVELOPER v20.2',
/* originating_system */ 'Autodesk Translation Framework v15.17.0.0',
/* authorisation */ '');

FILE_SCHEMA (('AUTOMOTIVE_DESIGN { 1 0 10303 214 3 1 1 }'));
ENDSEC;

DATA;
#10=MECHANICAL_DESIGN_GEOMETRIC_PRESENTATION_REPRESENTATION('',(#293),#7425);
#206=CONICAL_SURFACE('',#4672,0.275,0.785398163397449);
#241=SHAPE_REPRESENTATION_RELATIONSHIP('SRR','None',#7551,#267);
#267=ADVANCED_BREP_SHAPE_REPRESENTATION('',(#318),#7414);
#293=STYLED_ITEM('',(#7751),#318);
#318=MANIFOLD_SOLID_BREP('Body1',#4099);
#401=FACE_BOUND('',#1037,.T.);
#402=FACE_BOUND('',#1040,.T.);
#494=PLANE('',#4677);
#495=PLANE('',#4681);
#715=FACE_OUTER_BOUND('',#1034,.T.);
#716=FACE_OUTER_BOUND('',#1035,.T.);
#717=FACE_OUTER_BOUND('',#1036,.T.);
#718=FACE_OUTER_BOUND('',#1038,.T.);
#719=FACE_OUTER_BOUND('',#1039,.T.);
#1034=EDGE_LOOP('',(#3303,#3304,#3305,#3306));
#1035=EDGE_LOOP('',(#3307,#3308,#3309,#3310));
#1036=EDGE_LOOP('',(#3311));
#1037=EDGE_LOOP('',(#3312));
#1038=EDGE_LOOP('',(#3313,#3314,#3315,#3316));
#1039=EDGE_LOOP('',(#3317));
#1040=EDGE_LOOP('',(#3318));
#1310=LINE('',#6799,#1618);
#1311=LINE('',#6803,#1619);
#1312=LINE('',#6810,#1620);
#1618=VECTOR('',#5593,0.275);
#1619=VECTOR('',#5598,0.265);
#1620=VECTOR('',#5607,0.5);
#1900=CIRCLE('',#4673,0.285);
#1901=CIRCLE('',#4674,0.265);
#1902=CIRCLE('',#4676,0.265);
#1903=CIRCLE('',#4678,0.5);
#1904=CIRCLE('',#4680,0.5);
#2132=VERTEX_POINT('',#6796);
#2133=VERTEX_POINT('',#6798);
#2134=VERTEX_POINT('',#6802);
#2135=VERTEX_POINT('',#6806);
#2136=VERTEX_POINT('',#6809);
#2544=EDGE_CURVE('',#2132,#2132,#1900,.T.);
#2545=EDGE_CURVE('',#2132,#2133,#1310,.T.);
#2546=EDGE_CURVE('',#2133,#2133,#1901,.T.);
#2547=EDGE_CURVE('',#2133,#2134,#1311,.T.);
#2548=EDGE_CURVE('',#2134,#2134,#1902,.T.);
#2549=EDGE_CURVE('',#2135,#2135,#1903,.T.);
#2550=EDGE_CURVE('',#2135,#2136,#1312,.T.);
#2551=EDGE_CURVE('',#2136,#2136,#1904,.T.);
#3303=ORIENTED_EDGE('',*,*,#2544,.T.);
#3304=ORIENTED_EDGE('',*,*,#2545,.T.);
#3305=ORIENTED_EDGE('',*,*,#2546,.T.);
#3306=ORIENTED_EDGE('',*,*,#2545,.F.);
#3307=ORIENTED_EDGE('',*,*,#2546,.F.);
#3308=ORIENTED_EDGE('',*,*,#2547,.T.);
#3309=ORIENTED_EDGE('',*,*,#2548,.T.);
#3310=ORIENTED_EDGE('',*,*,#2547,.F.);
#3311=ORIENTED_EDGE('',*,*,#2549,.T.);
#3312=ORIENTED_EDGE('',*,*,#2544,.F.);
#3313=ORIENTED_EDGE('',*,*,#2549,.F.);
#3314=ORIENTED_EDGE('',*,*,#2550,.T.);
#3315=ORIENTED_EDGE('',*,*,#2551,.T.);
#3316=ORIENTED_EDGE('',*,*,#2550,.F.);
#3317=ORIENTED_EDGE('',*,*,#2551,.F.);
#3318=ORIENTED_EDGE('',*,*,#2548,.F.);
#3818=CYLINDRICAL_SURFACE('',#4675,0.265);
#3819=CYLINDRICAL_SURFACE('',#4679,0.5);
#3969=ADVANCED_FACE('',(#715),#206,.F.);
#3970=ADVANCED_FACE('',(#716),#3818,.F.);
#3971=ADVANCED_FACE('',(#717,#401),#494,.T.);
#3972=ADVANCED_FACE('',(#718),#3819,.T.);
#3973=ADVANCED_FACE('',(#719,#402),#495,.F.);
#4099=CLOSED_SHELL('',(#3969,#3970,#3971,#3972,#3973));
#4671=AXIS2_PLACEMENT_3D('',#6794,#5587,#5588);
#4672=AXIS2_PLACEMENT_3D('',#6795,#5589,#5590);
#4673=AXIS2_PLACEMENT_3D('',#6797,#5591,#5592);
#4674=AXIS2_PLACEMENT_3D('',#6800,#5594,#5595);
#4675=AXIS2_PLACEMENT_3D('',#6801,#5596,#5597);
#4676=AXIS2_PLACEMENT_3D('',#6804,#5599,#5600);
#4677=AXIS2_PLACEMENT_3D('',#6805,#5601,#5602);
#4678=AXIS2_PLACEMENT_3D('',#6807,#5603,#5604);
#4679=AXIS2_PLACEMENT_3D('',#6808,#5605,#5606);
#4680=AXIS2_PLACEMENT_3D('',#6811,#5608,#5609);
#4681=AXIS2_PLACEMENT_3D('',#6812,#5610,#5611);
#5587=DIRECTION('axis',(0.,0.,1.));
#5588=DIRECTION('refdir',(1.,0.,0.));
#5589=DIRECTION('center_axis',(0.,1.,0.));
#5590=DIRECTION('ref_axis',(1.,0.,0.));
#5591=DIRECTION('center_axis',(0.,1.,0.));
#5592=DIRECTION('ref_axis',(1.,0.,0.));
#5593=DIRECTION('',(0.707106781186548,-0.707106781186547,-8.65956056235494E-17));
#5594=DIRECTION('center_axis',(0.,-1.,0.));
#5595=DIRECTION('ref_axis',(1.,0.,0.));
#5596=DIRECTION('center_axis',(0.,1.,0.));
#5597=DIRECTION('ref_axis',(1.,0.,0.));
#5598=DIRECTION('',(0.,-1.,0.));
#5599=DIRECTION('center_axis',(0.,-1.,0.));
#5600=DIRECTION('ref_axis',(1.,0.,0.));
#5601=DIRECTION('center_axis',(0.,1.,0.));
#5602=DIRECTION('ref_axis',(1.,0.,0.));
#5603=DIRECTION('center_axis',(0.,1.,0.));
#5604=DIRECTION('ref_axis',(1.,0.,0.));
#5605=DIRECTION('center_axis',(0.,1.,0.));
#5606=DIRECTION('ref_axis',(1.,0.,0.));
#5607=DIRECTION('',(0.,-1.,0.));
#5608=DIRECTION('center_axis',(0.,1.,0.));
#5609=DIRECTION('ref_axis',(1.,0.,0.));
#5610=DIRECTION('center_axis',(0.,1.,0.));
#5611=DIRECTION('ref_axis',(1.,0.,0.));
#6794=CARTESIAN_POINT('',(0.,0.,0.));
#6795=CARTESIAN_POINT('Origin',(0.,0.09,0.));
#6796=CARTESIAN_POINT('',(-0.285,0.1,3.49024337756996E-17));
#6797=CARTESIAN_POINT('Origin',(0.,0.1,0.));
#6798=CARTESIAN_POINT('',(-0.265,0.08,-3.24531401774049E-17));
#6799=CARTESIAN_POINT('',(-0.275,0.09,3.36777869765522E-17));
#6800=CARTESIAN_POINT('Origin',(0.,0.08,0.));
#6801=CARTESIAN_POINT('Origin',(0.,0.,0.));
#6802=CARTESIAN_POINT('',(-0.265,0.,3.24531401774049E-17));
#6803=CARTESIAN_POINT('',(-0.265,0.,3.24531401774049E-17));
#6804=CARTESIAN_POINT('Origin',(0.,0.,0.));
#6805=CARTESIAN_POINT('Origin',(0.,0.1,0.));
#6806=CARTESIAN_POINT('',(-0.5,0.1,6.12323399573677E-17));
#6807=CARTESIAN_POINT('Origin',(0.,0.1,0.));
#6808=CARTESIAN_POINT('Origin',(0.,0.,0.));
#6809=CARTESIAN_POINT('',(-0.5,0.,6.12323399573677E-17));
#6810=CARTESIAN_POINT('',(-0.5,0.,6.12323399573677E-17));
#6811=CARTESIAN_POINT('Origin',(0.,0.,0.));
#6812=CARTESIAN_POINT('Origin',(0.,0.,0.));
#7384=UNCERTAINTY_MEASURE_WITH_UNIT(LENGTH_MEASURE(0.001),#7426,
'DISTANCE_ACCURACY_VALUE',
'Maximum model space distance between geometric entities at asserted c
onnectivities');
#7395=UNCERTAINTY_MEASURE_WITH_UNIT(LENGTH_MEASURE(0.001),#7426,
'DISTANCE_ACCURACY_VALUE',
'Maximum model space distance between geometric entities at asserted c
onnectivities');
#7414=(
GEOMETRIC_REPRESENTATION_CONTEXT(3)
GLOBAL_UNCERTAINTY_ASSIGNED_CONTEXT((#7384))
GLOBAL_UNIT_ASSIGNED_CONTEXT((#7426,#7428,#7429))
REPRESENTATION_CONTEXT('','3D')
);
#7425=(
GEOMETRIC_REPRESENTATION_CONTEXT(3)
GLOBAL_UNCERTAINTY_ASSIGNED_CONTEXT((#7395))
GLOBAL_UNIT_ASSIGNED_CONTEXT((#7426,#7428,#7429))
REPRESENTATION_CONTEXT('','3D')
);
#7426=(
LENGTH_UNIT()
NAMED_UNIT(*)
SI_UNIT(.CENTI.,.METRE.)
);
#7428=(
NAMED_UNIT(*)
PLANE_ANGLE_UNIT()
SI_UNIT($,.RADIAN.)
);
#7429=(
NAMED_UNIT(*)
SI_UNIT($,.STERADIAN.)
SOLID_ANGLE_UNIT()
);
#7448=SHAPE_DEFINITION_REPRESENTATION(#7477,#7551);
#7477=PRODUCT_DEFINITION_SHAPE('',$,#7581);
#7551=SHAPE_REPRESENTATION('',(#4671),#7414);
#7562=PRODUCT_DEFINITION_CONTEXT('part definition',#7651,'design');
#7581=PRODUCT_DEFINITION('Flat Washer - M5','Flat Washer - M5',#7610,#7562);
#7610=PRODUCT_DEFINITION_FORMATION('',$,#7671);
#7651=APPLICATION_CONTEXT(
'Core Data for Automotive Mechanical Design Process');
#7652=PRODUCT_CONTEXT('part definition',#7651,'mechanical');
#7671=PRODUCT('Flat Washer - M5','Flat Washer - M5','Flat Washer - M5',
(#7652));
#7745=COLOUR_RGB('Black',0.12,0.14,0.17);
#7746=FILL_AREA_STYLE_COLOUR('',#7745);
#7747=FILL_AREA_STYLE('',(#7746));
#7748=SURFACE_STYLE_FILL_AREA(#7747);
#7749=SURFACE_SIDE_STYLE('',(#7748));
#7750=SURFACE_STYLE_USAGE(.BOTH.,#7749);
#7751=PRESENTATION_STYLE_ASSIGNMENT((#7750));
ENDSEC;
END-ISO-10303-21;
